ISO-10303-21;
HEADER;
/* Generated by software containing ST-Developer
 * from STEP Tools, Inc. (www.steptools.com) 
 */

FILE_DESCRIPTION(
/* description */ ('Low-profile wedge edge clamp'),
/* implementation_level */ '2;1');

FILE_NAME(
/* name */ 'M5x14 Cap Screw.step',
/* time_stamp */ '2026-10-29T15:58:13-07:00',
/* author */ (''),
/* organization */ (''),
/* preprocessor_version */ 'ST-DEVELOPER v20.2',
/* originating_system */ 'Autodesk Translation Framework v15.17.0.0',
/* authorisation */ '');

FILE_SCHEMA (('AUTOMOTIVE_DESIGN { 1 0 10303 214 3 1 1 }'));
ENDSEC;

DATA;
#10=MECHANICAL_DESIGN_GEOMETRIC_PRESENTATION_REPRESENTATION('',(#82),#2996);
#57=CONICAL_SURFACE('',#1935,0.4,0.785398163397448);
#58=CONICAL_SURFACE('',#1939,0.41,0.785398163397448);
#59=CONICAL_SURFACE('',#1943,0.26,0.463647609000806);
#62=ORIENTED_CLOSED_SHELL('',*,#1711,.F.);
#63=BREP_WITH_VOIDS('Body1',#1712,(#62));
#70=SHAPE_REPRESENTATION_RELATIONSHIP('SRR','None',#3032,#76);
#76=ADVANCED_BREP_SHAPE_REPRESENTATION('',(#63),#2993);
#82=STYLED_ITEM('',(#3133),#63);
#158=FACE_BOUND('',#444,.T.);
#186=PLANE('',#1923);
#187=PLANE('',#1924);
#188=PLANE('',#1925);
#189=PLANE('',#1926);
#190=PLANE('',#1927);
#191=PLANE('',#1928);
#192=PLANE('',#1929);
#193=PLANE('',#1930);
#194=PLANE('',#1931);
#195=PLANE('',#1933);
#196=PLANE('',#1941);
#269=FACE_OUTER_BOUND('',#430,.T.);
#270=FACE_OUTER_BOUND('',#431,.T.);
#271=FACE_OUTER_BOUND('',#432,.T.);
#272=FACE_OUTER_BOUND('',#433,.T.);
#273=FACE_OUTER_BOUND('',#434,.T.);
#274=FACE_OUTER_BOUND('',#435,.T.);
#275=FACE_OUTER_BOUND('',#436,.T.);
#276=FACE_OUTER_BOUND('',#437,.T.);
#277=FACE_OUTER_BOUND('',#438,.T.);
#278=FACE_OUTER_BOUND('',#439,.T.);
#279=FACE_OUTER_BOUND('',#440,.T.);
#280=FACE_OUTER_BOUND('',#441,.T.);
#281=FACE_OUTER_BOUND('',#442,.T.);
#282=FACE_OUTER_BOUND('',#443,.T.);
#283=FACE_OUTER_BOUND('',#445,.T.);
#284=FACE_OUTER_BOUND('',#446,.T.);
#430=EDGE_LOOP('',(#1451,#1452,#1453,#1454));
#431=EDGE_LOOP('',(#1455,#1456,#1457,#1458));
#432=EDGE_LOOP('',(#1459,#1460,#1461,#1462));
#433=EDGE_LOOP('',(#1463,#1464,#1465,#1466));
#434=EDGE_LOOP('',(#1467,#1468,#1469,#1470));
#435=EDGE_LOOP('',(#1471,#1472,#1473,#1474));
#436=EDGE_LOOP('',(#1475,#1476,#1477,#1478,#1479,#1480));
#437=EDGE_LOOP('',(#1481,#1482,#1483,#1484,#1485,#1486));
#438=EDGE_LOOP('',(#1487));
#439=EDGE_LOOP('',(#1488));
#440=EDGE_LOOP('',(#1489,#1490,#1491,#1492));
#441=EDGE_LOOP('',(#1493,#1494,#1495,#1496));
#442=EDGE_LOOP('',(#1497,#1498,#1499,#1500));
#443=EDGE_LOOP('',(#1501));
#444=EDGE_LOOP('',(#1502));
#445=EDGE_LOOP('',(#1503,#1504,#1505,#1506));
#446=EDGE_LOOP('',(#1507,#1508,#1509,#1510));
#545=LINE('',#2826,#664);
#546=LINE('',#2828,#665);
#547=LINE('',#2830,#666);
#548=LINE('',#2831,#667);
#549=LINE('',#2834,#668);
#550=LINE('',#2836,#669);
#551=LINE('',#2837,#670);
#552=LINE('',#2840,#671);
#553=LINE('',#2842,#672);
#554=LINE('',#2843,#673);
#555=LINE('',#2846,#674);
#556=LINE('',#2848,#675);
#557=LINE('',#2849,#676);
#558=LINE('',#2852,#677);
#559=LINE('',#2854,#678);
#560=LINE('',#2855,#679);
#561=LINE('',#2857,#680);
#562=LINE('',#2858,#681);
#563=LINE('',#2870,#682);
#564=LINE('',#2874,#683);
#565=LINE('',#2878,#684);
#566=LINE('',#2885,#685);
#567=LINE('',#2887,#686);
#664=VECTOR('',#2345,1.);
#665=VECTOR('',#2346,1.);
#666=VECTOR('',#2347,1.);
#667=VECTOR('',#2348,1.);
#668=VECTOR('',#2351,1.);
#669=VECTOR('',#2352,1.);
#670=VECTOR('',#2353,1.);
#671=VECTOR('',#2356,1.);
#672=VECTOR('',#2357,1.);
#673=VECTOR('',#2358,1.);
#674=VECTOR('',#2361,1.);
#675=VECTOR('',#2362,1.);
#676=VECTOR('',#2363,1.);
#677=VECTOR('',#2366,1.);
#678=VECTOR('',#2367,1.);
#679=VECTOR('',#2368,1.);
#680=VECTOR('',#2371,1.);
#681=VECTOR('',#2372,1.);
#682=VECTOR('',#2389,0.4);
#683=VECTOR('',#2394,0.425);
#684=VECTOR('',#2399,0.41);
#685=VECTOR('',#2408,0.26);
#686=VECTOR('',#2411,0.25);
#775=CIRCLE('',#1932,0.24505);
#776=CIRCLE('',#1934,0.375);
#777=CIRCLE('',#1936,0.425);
#778=CIRCLE('',#1938,0.425);
#779=CIRCLE('',#1940,0.395);
#780=CIRCLE('',#1942,0.27);
#781=CIRCLE('',#1944,0.24505);
#892=VERTEX_POINT('',#2824);
#893=VERTEX_POINT('',#2825);
#894=VERTEX_POINT('',#2827);
#895=VERTEX_POINT('',#2829);
#896=VERTEX_POINT('',#2833);
#897=VERTEX_POINT('',#2835);
#898=VERTEX_POINT('',#2839);
#899=VERTEX_POINT('',#2841);
#900=VERTEX_POINT('',#2845);
#901=VERTEX_POINT('',#2847);
#902=VERTEX_POINT('',#2851);
#903=VERTEX_POINT('',#2853);
#904=VERTEX_POINT('',#2862);
#905=VERTEX_POINT('',#2865);
#906=VERTEX_POINT('',#2868);
#907=VERTEX_POINT('',#2872);
#908=VERTEX_POINT('',#2876);
#909=VERTEX_POINT('',#2880);
#910=VERTEX_POINT('',#2883);
#1084=EDGE_CURVE('',#892,#893,#545,.T.);
#1085=EDGE_CURVE('',#893,#894,#546,.T.);
#1086=EDGE_CURVE('',#894,#895,#547,.T.);
#1087=EDGE_CURVE('',#892,#895,#548,.T.);
#1088=EDGE_CURVE('',#893,#896,#549,.T.);
#1089=EDGE_CURVE('',#896,#897,#550,.T.);
#1090=EDGE_CURVE('',#897,#894,#551,.T.);
#1091=EDGE_CURVE('',#896,#898,#552,.T.);
#1092=EDGE_CURVE('',#898,#899,#553,.T.);
#1093=EDGE_CURVE('',#899,#897,#554,.T.);
#1094=EDGE_CURVE('',#898,#900,#555,.T.);
#1095=EDGE_CURVE('',#900,#901,#556,.T.);
#1096=EDGE_CURVE('',#901,#899,#557,.T.);
#1097=EDGE_CURVE('',#900,#902,#558,.T.);
#1098=EDGE_CURVE('',#902,#903,#559,.T.);
#1099=EDGE_CURVE('',#903,#901,#560,.T.);
#1100=EDGE_CURVE('',#902,#892,#561,.T.);
#1101=EDGE_CURVE('',#895,#903,#562,.T.);
#1102=EDGE_CURVE('',#904,#904,#775,.T.);
#1103=EDGE_CURVE('',#905,#905,#776,.T.);
#1104=EDGE_CURVE('',#906,#906,#777,.T.);
#1105=EDGE_CURVE('',#906,#905,#563,.T.);
#1106=EDGE_CURVE('',#907,#907,#778,.T.);
#1107=EDGE_CURVE('',#907,#906,#564,.T.);
#1108=EDGE_CURVE('',#908,#908,#779,.T.);
#1109=EDGE_CURVE('',#908,#907,#565,.T.);
#1110=EDGE_CURVE('',#909,#909,#780,.T.);
#1111=EDGE_CURVE('',#910,#910,#781,.F.);
#1112=EDGE_CURVE('',#910,#909,#566,.T.);
#1113=EDGE_CURVE('',#904,#910,#567,.T.);
#1451=ORIENTED_EDGE('',*,*,#1084,.T.);
#1452=ORIENTED_EDGE('',*,*,#1085,.T.);
#1453=ORIENTED_EDGE('',*,*,#1086,.T.);
#1454=ORIENTED_EDGE('',*,*,#1087,.F.);
#1455=ORIENTED_EDGE('',*,*,#1088,.T.);
#1456=ORIENTED_EDGE('',*,*,#1089,.T.);
#1457=ORIENTED_EDGE('',*,*,#1090,.T.);
#1458=ORIENTED_EDGE('',*,*,#1085,.F.);
#1459=ORIENTED_EDGE('',*,*,#1091,.T.);
#1460=ORIENTED_EDGE('',*,*,#1092,.T.);
#1461=ORIENTED_EDGE('',*,*,#1093,.T.);
#1462=ORIENTED_EDGE('',*,*,#1089,.F.);
#1463=ORIENTED_EDGE('',*,*,#1094,.T.);
#1464=ORIENTED_EDGE('',*,*,#1095,.T.);
#1465=ORIENTED_EDGE('',*,*,#1096,.T.);
#1466=ORIENTED_EDGE('',*,*,#1092,.F.);
#1467=ORIENTED_EDGE('',*,*,#1097,.T.);
#1468=ORIENTED_EDGE('',*,*,#1098,.T.);
#1469=ORIENTED_EDGE('',*,*,#1099,.T.);
#1470=ORIENTED_EDGE('',*,*,#1095,.F.);
#1471=ORIENTED_EDGE('',*,*,#1100,.T.);
#1472=ORIENTED_EDGE('',*,*,#1087,.T.);
#1473=ORIENTED_EDGE('',*,*,#1101,.T.);
#1474=ORIENTED_EDGE('',*,*,#1098,.F.);
#1475=ORIENTED_EDGE('',*,*,#1100,.F.);
#1476=ORIENTED_EDGE('',*,*,#1097,.F.);
#1477=ORIENTED_EDGE('',*,*,#1094,.F.);
#1478=ORIENTED_EDGE('',*,*,#1091,.F.);
#1479=ORIENTED_EDGE('',*,*,#1088,.F.);
#1480=ORIENTED_EDGE('',*,*,#1084,.F.);
#1481=ORIENTED_EDGE('',*,*,#1101,.F.);
#1482=ORIENTED_EDGE('',*,*,#1086,.F.);
#1483=ORIENTED_EDGE('',*,*,#1090,.F.);
#1484=ORIENTED_EDGE('',*,*,#1093,.F.);
#1485=ORIENTED_EDGE('',*,*,#1096,.F.);
#1486=ORIENTED_EDGE('',*,*,#1099,.F.);
#1487=ORIENTED_EDGE('',*,*,#1102,.F.);
#1488=ORIENTED_EDGE('',*,*,#1103,.F.);
#1489=ORIENTED_EDGE('',*,*,#1104,.F.);
#1490=ORIENTED_EDGE('',*,*,#1105,.T.);
#1491=ORIENTED_EDGE('',*,*,#1103,.T.);
#1492=ORIENTED_EDGE('',*,*,#1105,.F.);
#1493=ORIENTED_EDGE('',*,*,#1106,.F.);
#1494=ORIENTED_EDGE('',*,*,#1107,.T.);
#1495=ORIENTED_EDGE('',*,*,#1104,.T.);
#1496=ORIENTED_EDGE('',*,*,#1107,.F.);
#1497=ORIENTED_EDGE('',*,*,#1108,.F.);
#1498=ORIENTED_EDGE('',*,*,#1109,.T.);
#1499=ORIENTED_EDGE('',*,*,#1106,.T.);
#1500=ORIENTED_EDGE('',*,*,#1109,.F.);
#1501=ORIENTED_EDGE('',*,*,#1108,.T.);
#1502=ORIENTED_EDGE('',*,*,#1110,.F.);
#1503=ORIENTED_EDGE('',*,*,#1111,.F.);
#1504=ORIENTED_EDGE('',*,*,#1112,.T.);
#1505=ORIENTED_EDGE('',*,*,#1110,.T.);
#1506=ORIENTED_EDGE('',*,*,#1112,.F.);
#1507=ORIENTED_EDGE('',*,*,#1102,.T.);
#1508=ORIENTED_EDGE('',*,*,#1113,.T.);
#1509=ORIENTED_EDGE('',*,*,#1111,.T.);
#1510=ORIENTED_EDGE('',*,*,#1113,.F.);
#1610=CYLINDRICAL_SURFACE('',#1937,0.425);
#1611=CYLINDRICAL_SURFACE('',#1945,0.24505);
#1676=ADVANCED_FACE('',(#269),#186,.F.);
#1677=ADVANCED_FACE('',(#270),#187,.F.);
#1678=ADVANCED_FACE('',(#271),#188,.F.);
#1679=ADVANCED_FACE('',(#272),#189,.F.);
#1680=ADVANCED_FACE('',(#273),#190,.F.);
#1681=ADVANCED_FACE('',(#274),#191,.F.);
#1682=ADVANCED_FACE('',(#275),#192,.F.);
#1683=ADVANCED_FACE('',(#276),#193,.F.);
#1684=ADVANCED_FACE('',(#277),#194,.F.);
#1685=ADVANCED_FACE('',(#278),#195,.T.);
#1686=ADVANCED_FACE('',(#279),#57,.T.);
#1687=ADVANCED_FACE('',(#280),#1610,.T.);
#1688=ADVANCED_FACE('',(#281),#58,.T.);
#1689=ADVANCED_FACE('',(#282,#158),#196,.T.);
#1690=ADVANCED_FACE('',(#283),#59,.T.);
#1691=ADVANCED_FACE('',(#284),#1611,.T.);
#1711=CLOSED_SHELL('',(#1676,#1677,#1678,#1679,#1680,#1681,#1682,#1683));
#1712=CLOSED_SHELL('',(#1684,#1685,#1686,#1687,#1688,#1689,#1690,#1691));
#1922=AXIS2_PLACEMENT_3D('',#2822,#2341,#2342);
#1923=AXIS2_PLACEMENT_3D('',#2823,#2343,#2344);
#1924=AXIS2_PLACEMENT_3D('',#2832,#2349,#2350);
#1925=AXIS2_PLACEMENT_3D('',#2838,#2354,#2355);
#1926=AXIS2_PLACEMENT_3D('',#2844,#2359,#2360);
#1927=AXIS2_PLACEMENT_3D('',#2850,#2364,#2365);
#1928=AXIS2_PLACEMENT_3D('',#2856,#2369,#2370);
#1929=AXIS2_PLACEMENT_3D('',#2859,#2373,#2374);
#1930=AXIS2_PLACEMENT_3D('',#2860,#2375,#2376);
#1931=AXIS2_PLACEMENT_3D('',#2861,#2377,#2378);
#1932=AXIS2_PLACEMENT_3D('',#2863,#2379,#2380);
#1933=AXIS2_PLACEMENT_3D('',#2864,#2381,#2382);
#1934=AXIS2_PLACEMENT_3D('',#2866,#2383,#2384);
#1935=AXIS2_PLACEMENT_3D('',#2867,#2385,#2386);
#1936=AXIS2_PLACEMENT_3D('',#2869,#2387,#2388);
#1937=AXIS2_PLACEMENT_3D('',#2871,#2390,#2391);
#1938=AXIS2_PLACEMENT_3D('',#2873,#2392,#2393);
#1939=AXIS2_PLACEMENT_3D('',#2875,#2395,#2396);
#1940=AXIS2_PLACEMENT_3D('',#2877,#2397,#2398);
#1941=AXIS2_PLACEMENT_3D('',#2879,#2400,#2401);
#1942=AXIS2_PLACEMENT_3D('',#2881,#2402,#2403);
#1943=AXIS2_PLACEMENT_3D('',#2882,#2404,#2405);
#1944=AXIS2_PLACEMENT_3D('',#2884,#2406,#2407);
#1945=AXIS2_PLACEMENT_3D('',#2886,#2409,#2410);
#2341=DIRECTION('axis',(0.,0.,1.));
#2342=DIRECTION('refdir',(1.,0.,0.));
#2343=DIRECTION('center_axis',(0.866025403784439,0.,-0.5));
#2344=DIRECTION('ref_axis',(0.5,0.,0.866025403784439));
#2345=DIRECTION('',(-0.5,0.,-0.866025403784439));
#2346=DIRECTION('',(0.,-1.,0.));
#2347=DIRECTION('',(0.5,0.,0.866025403784439));
#2348=DIRECTION('',(0.,-1.,0.));
#2349=DIRECTION('center_axis',(1.20185167898973E-16,0.,-1.));
#2350=DIRECTION('ref_axis',(1.,0.,1.20185167898973E-16));
#2351=DIRECTION('',(-1.,0.,-1.20185167898973E-16));
#2352=DIRECTION('',(0.,-1.,0.));
#2353=DIRECTION('',(1.,0.,1.20185167898973E-16));
#2354=DIRECTION('center_axis',(-0.866025403784439,0.,-0.5));
#2355=DIRECTION('ref_axis',(0.5,0.,-0.866025403784439));
#2356=DIRECTION('',(-0.5,0.,0.866025403784439));
#2357=DIRECTION('',(0.,-1.,0.));
#2358=DIRECTION('',(0.5,0.,-0.866025403784439));
#2359=DIRECTION('center_axis',(-0.866025403784439,0.,0.5));
#2360=DIRECTION('ref_axis',(-0.5,0.,-0.866025403784439));
#2361=DIRECTION('',(0.5,0.,0.866025403784439));
#2362=DIRECTION('',(0.,-1.,0.));
#2363=DIRECTION('',(-0.5,0.,-0.866025403784439));
#2364=DIRECTION('center_axis',(-2.40370335797945E-16,0.,1.));
#2365=DIRECTION('ref_axis',(-1.,0.,-2.40370335797945E-16));
#2366=DIRECTION('',(1.,0.,2.40370335797945E-16));
#2367=DIRECTION('',(0.,-1.,0.));
#2368=DIRECTION('',(-1.,0.,-2.40370335797945E-16));
#2369=DIRECTION('center_axis',(0.866025403784439,0.,0.5));
#2370=DIRECTION('ref_axis',(-0.5,0.,0.866025403784439));
#2371=DIRECTION('',(0.5,0.,-0.866025403784439));
#2372=DIRECTION('',(-0.5,0.,0.866025403784439));
#2373=DIRECTION('center_axis',(0.,1.,0.));
#2374=DIRECTION('ref_axis',(1.,0.,0.));
#2375=DIRECTION('center_axis',(0.,-1.,0.));
#2376=DIRECTION('ref_axis',(0.,0.,-1.));
#2377=DIRECTION('center_axis',(0.,1.,0.));
#2378=DIRECTION('ref_axis',(1.,0.,0.));
#2379=DIRECTION('center_axis',(0.,1.,0.));
#2380=DIRECTION('ref_axis',(1.,0.,0.));
#2381=DIRECTION('center_axis',(0.,1.,0.));
#2382=DIRECTION('ref_axis',(0.,0.,1.));
#2383=DIRECTION('center_axis',(0.,-1.,0.));
#2384=DIRECTION('ref_axis',(1.,0.,0.));
#2385=DIRECTION('center_axis',(0.,-1.,0.));
#2386=DIRECTION('ref_axis',(1.,0.,0.));
#2387=DIRECTION('center_axis',(0.,-1.,0.));
#2388=DIRECTION('ref_axis',(1.,0.,0.));
#2389=DIRECTION('',(0.707106781186548,0.707106781186547,8.65956056235493E-17));
#2390=DIRECTION('center_axis',(0.,-1.,0.));
#2391=DIRECTION('ref_axis',(1.,0.,0.));
#2392=DIRECTION('center_axis',(0.,-1.,0.));
#2393=DIRECTION('ref_axis',(1.,0.,0.));
#2394=DIRECTION('',(0.,1.,0.));
#2395=DIRECTION('center_axis',(0.,1.,0.));
#2396=DIRECTION('ref_axis',(1.,0.,0.));
#2397=DIRECTION('center_axis',(0.,-1.,0.));
#2398=DIRECTION('ref_axis',(1.,0.,0.));
#2399=DIRECTION('',(-0.707106781186547,0.707106781186548,-8.65956056235493E-17));
#2400=DIRECTION('center_axis',(0.,-1.,0.));
#2401=DIRECTION('ref_axis',(0.,0.,-1.));
#2402=DIRECTION('center_axis',(0.,-1.,0.));
#2403=DIRECTION('ref_axis',(1.,0.,0.));
#2404=DIRECTION('center_axis',(0.,1.,0.));
#2405=DIRECTION('ref_axis',(1.,0.,0.));
#2406=DIRECTION('center_axis',(0.,1.,0.));
#2407=DIRECTION('ref_axis',(1.,0.,0.));
#2408=DIRECTION('',(-0.447213595499958,0.894427190999916,-5.47678698264203E-17));
#2409=DIRECTION('center_axis',(0.,-1.,0.));
#2410=DIRECTION('ref_axis',(1.,0.,0.));
#2411=DIRECTION('',(0.,1.,0.));
#2822=CARTESIAN_POINT('',(0.,0.,0.));
#2823=CARTESIAN_POINT('Origin',(0.115470053837925,-0.5,-0.2));
#2824=CARTESIAN_POINT('',(0.23094010767585,-0.5,0.));
#2825=CARTESIAN_POINT('',(0.115470053837925,-0.5,-0.2));
#2826=CARTESIAN_POINT('',(0.23094010767585,-0.5,0.));
#2827=CARTESIAN_POINT('',(0.115470053837925,-0.8,-0.2));
#2828=CARTESIAN_POINT('',(0.115470053837925,-0.5,-0.2));
#2829=CARTESIAN_POINT('',(0.23094010767585,-0.8,0.));
#2830=CARTESIAN_POINT('',(0.23094010767585,-0.8,0.));
#2831=CARTESIAN_POINT('',(0.23094010767585,-0.5,0.));
#2832=CARTESIAN_POINT('Origin',(-0.115470053837925,-0.5,-0.2));
#2833=CARTESIAN_POINT('',(-0.115470053837925,-0.5,-0.2));
#2834=CARTESIAN_POINT('',(0.115470053837925,-0.5,-0.2));
#2835=CARTESIAN_POINT('',(-0.115470053837925,-0.8,-0.2));
#2836=CARTESIAN_POINT('',(-0.115470053837925,-0.5,-0.2));
#2837=CARTESIAN_POINT('',(0.115470053837925,-0.8,-0.2));
#2838=CARTESIAN_POINT('Origin',(-0.23094010767585,-0.5,-2.77555756156289E-17));
#2839=CARTESIAN_POINT('',(-0.23094010767585,-0.5,-2.82820063659975E-17));
#2840=CARTESIAN_POINT('',(-0.115470053837925,-0.5,-0.2));
#2841=CARTESIAN_POINT('',(-0.23094010767585,-0.8,-2.77555756156289E-17));
#2842=CARTESIAN_POINT('',(-0.23094010767585,-0.5,-2.82820063659975E-17));
#2843=CARTESIAN_POINT('',(-0.115470053837925,-0.8,-0.2));
#2844=CARTESIAN_POINT('Origin',(-0.115470053837925,-0.5,0.2));
#2845=CARTESIAN_POINT('',(-0.115470053837925,-0.5,0.2));
#2846=CARTESIAN_POINT('',(-0.23094010767585,-0.5,-2.82820063659975E-17));
#2847=CARTESIAN_POINT('',(-0.115470053837925,-0.8,0.2));
#2848=CARTESIAN_POINT('',(-0.115470053837925,-0.5,0.2));
#2849=CARTESIAN_POINT('',(-0.23094010767585,-0.8,-2.82820063659975E-17));
#2850=CARTESIAN_POINT('Origin',(0.115470053837925,-0.5,0.2));
#2851=CARTESIAN_POINT('',(0.115470053837925,-0.5,0.2));
#2852=CARTESIAN_POINT('',(-0.115470053837925,-0.5,0.2));
#2853=CARTESIAN_POINT('',(0.115470053837925,-0.8,0.2));
#2854=CARTESIAN_POINT('',(0.115470053837925,-0.5,0.2));
#2855=CARTESIAN_POINT('',(-0.115470053837925,-0.8,0.2));
#2856=CARTESIAN_POINT('Origin',(0.23094010767585,-0.5,0.));
#2857=CARTESIAN_POINT('',(0.115470053837925,-0.5,0.2));
#2858=CARTESIAN_POINT('',(0.115470053837925,-0.8,0.2));
#2859=CARTESIAN_POINT('Origin',(0.,-0.5,0.));
#2860=CARTESIAN_POINT('Origin',(0.,-0.8,0.));
#2861=CARTESIAN_POINT('Origin',(0.,-1.4,0.));
#2862=CARTESIAN_POINT('',(-0.24505,-1.4,3.00099698131059E-17));
#2863=CARTESIAN_POINT('Origin',(0.,-1.4,0.));
#2864=CARTESIAN_POINT('Origin',(0.375,0.5,0.));
#2865=CARTESIAN_POINT('',(-0.375,0.5,-4.59242549680257E-17));
#2866=CARTESIAN_POINT('Origin',(0.,0.5,0.));
#2867=CARTESIAN_POINT('Origin',(0.,0.475,0.));
#2868=CARTESIAN_POINT('',(-0.425,0.45,-5.20474889637625E-17));
#2869=CARTESIAN_POINT('Origin',(0.,0.45,0.));
#2870=CARTESIAN_POINT('',(-0.4,0.475,-4.89858719658941E-17));
#2871=CARTESIAN_POINT('Origin',(0.,0.24,0.));
#2872=CARTESIAN_POINT('',(-0.425,0.0299999999999998,-5.20474889637625E-17));
#2873=CARTESIAN_POINT('Origin',(0.,0.0299999999999998,0.));
#2874=CARTESIAN_POINT('',(-0.425,0.24,-5.20474889637625E-17));
#2875=CARTESIAN_POINT('Origin',(0.,0.0150000000000001,0.));
#2876=CARTESIAN_POINT('',(-0.395,4.85722573273506E-17,-4.83735485663204E-17));
#2877=CARTESIAN_POINT('Origin',(0.,0.,0.));
#2878=CARTESIAN_POINT('',(-0.41,0.0150000000000001,-5.02105187650415E-17));
#2879=CARTESIAN_POINT('Origin',(0.27,0.,0.));
#2880=CARTESIAN_POINT('',(-0.27,0.,-3.30654635769785E-17));
#2881=CARTESIAN_POINT('Origin',(0.,0.,0.));
#2882=CARTESIAN_POINT('Origin',(0.,-0.02,0.));
#2883=CARTESIAN_POINT('',(-0.24505,-0.0498999999999999,3.00099698131059E-17));
#2884=CARTESIAN_POINT('Origin',(0.,-0.0498999999999999,0.));
#2885=CARTESIAN_POINT('',(-0.26,-0.02,-3.18408167778312E-17));
#2886=CARTESIAN_POINT('Origin',(0.,-0.995,0.));
#2887=CARTESIAN_POINT('',(-0.24505,-0.995,-3.00099698131059E-17));
#2984=UNCERTAINTY_MEASURE_WITH_UNIT(LENGTH_MEASURE(0.001),#2997,
'DISTANCE_ACCURACY_VALUE',
'Maximum model space distance between geometric entities at asserted c
onnectivities');
#2987=UNCERTAINTY_MEASURE_WITH_UNIT(LENGTH_MEASURE(0.001),#2997,
'DISTANCE_ACCURACY_VALUE',
'Maximum model space distance between geometric entities at asserted c
onnectivities');
#2993=(
GEOMETRIC_REPRESENTATION_CONTEXT(3)
GLOBAL_UNCERTAINTY_ASSIGNED_CONTEXT((#2984))
GLOBAL_UNIT_ASSIGNED_CONTEXT((#2997,#2999,#3000))
REPRESENTATION_CONTEXT('','3D')
);
#2996=(
GEOMETRIC_REPRESENTATION_CONTEXT(3)
GLOBAL_UNCERTAINTY_ASSIGNED_CONTEXT((#2987))
GLOBAL_UNIT_ASSIGNED_CONTEXT((#2997,#2999,#3000))
REPRESENTATION_CONTEXT('','3D')
);
#2997=(
LENGTH_UNIT()
NAMED_UNIT(*)
SI_UNIT(.CENTI.,.METRE.)
);
#2999=(
NAMED_UNIT(*)
PLANE_ANGLE_UNIT()
SI_UNIT($,.RADIAN.)
);
#3000=(
NAMED_UNIT(*)
SI_UNIT($,.STERADIAN.)
SOLID_ANGLE_UNIT()
);
#3006=SHAPE_DEFINITION_REPRESENTATION(#3014,#3032);
#3014=PRODUCT_DEFINITION_SHAPE('',$,#3041);
#3032=SHAPE_REPRESENTATION('',(#1922),#2993);
#3035=PRODUCT_DEFINITION_CONTEXT('part definition',#3061,'design');
#3041=PRODUCT_DEFINITION('M5x14 Cap Screw','M5x14 Cap Screw',#3049,#3035);
#3049=PRODUCT_DEFINITION_FORMATION('',$,#3068);
#3061=APPLICATION_CONTEXT(
'Core Data for Automotive Mechanical Design Process');
#3062=PRODUCT_CONTEXT('part definition',#3061,'mechanical');
#3068=PRODUCT('M5x14 Cap Screw','M5x14 Cap Screw','M5x14 Cap Screw',(#3062));
#3127=COLOUR_RGB('Black',0.12,0.14,0.17);
#3128=FILL_AREA_STYLE_COLOUR('',#3127);
#3129=FILL_AREA_STYLE('',(#3128));
#3130=SURFACE_STYLE_FILL_AREA(#3129);
#3131=SURFACE_SIDE_STYLE('',(#3130));
#3132=SURFACE_STYLE_USAGE(.BOTH.,#3131);
#3133=PRESENTATION_STYLE_ASSIGNMENT((#3132));
ENDSEC;
END-ISO-10303-21;
